ISO-10303-21;
HEADER;
FILE_DESCRIPTION (('STEP AP214'),
    '1' );
FILE_NAME ('socket head cap screw_iso_ISO 4762 M5 x 20 - 20N.step',
    '2026-10-08T05:45:04',
    ( '' ),
    ( '' ),
    'SwSTEP 2.0',
    'SolidWorks 2026',
    '' );
FILE_SCHEMA (( 'AUTOMOTIVE_DESIGN' ));
ENDSEC;

DATA;
#21=LINE ( 'NONE', #8698, #9426 ) ;
#27=VECTOR ( 'NONE', #4855, 1000.000000000000000 ) ;
#43=ORIENTED_EDGE ( 'NONE', *, *, #6494, .F. ) ;
#91=AXIS2_PLACEMENT_3D ( 'NONE', #3480, #6860, #2653 ) ;
#94=AXIS2_PLACEMENT_3D ( 'NONE', #6317, #9708, #415 ) ;
#150=DIRECTION ( 'NONE',  ( -1.000000000000000000, -0.000000000000000000, -0.000000000000000000 ) ) ;
#151=VECTOR ( 'NONE', #2662, 1000.000000000000000 ) ;
#211=AXIS2_PLACEMENT_3D ( 'NONE', #8616, #9603, #2730 ) ;
#257=AXIS2_PLACEMENT_3D ( 'NONE', #5414, #5255, #8742 ) ;
#275=CARTESIAN_POINT ( 'NONE',  ( 2.500000000000000000, 0.000000000000000000, 0.000000000000000000 ) ) ;
#308=AXIS2_PLACEMENT_3D ( 'NONE', #6956, #4296, #9565 ) ;
#318=VERTEX_POINT ( 'NONE', #2131 ) ;
#319=FACE_OUTER_BOUND ( 'NONE', #5879, .T. ) ;
#330=ORIENTED_EDGE ( 'NONE', *, *, #4103, .T. ) ;
#347=DIRECTION ( 'NONE',  ( 0.000000000000000000, 1.000000000000000000, -1.471414886128461471E-15 ) ) ;
#353=ORIENTED_EDGE ( 'NONE', *, *, #8457, .F. ) ;
#370=ORIENTED_EDGE ( 'NONE', *, *, #1853, .F. ) ;
#380=DIRECTION ( 'NONE',  ( 0.000000000000000000, 0.000000000000000000, 1.000000000000000000 ) ) ;
#383=ORIENTED_EDGE ( 'NONE', *, *, #9617, .T. ) ;
#397=DIRECTION ( 'NONE',  ( -1.000000000000000000, -0.000000000000000000, -0.000000000000000000 ) ) ;
#408=LINE ( 'NONE', #8607, #638 ) ;
#415=DIRECTION ( 'NONE',  ( 0.000000000000000000, 0.4999999999999993894, -0.8660254037844389297 ) ) ;
#422=PLANE ( 'NONE',  #6643 ) ;
#456=DIRECTION ( 'NONE',  ( 0.000000000000000000, -1.000000000000000000, 1.287488025362403787E-15 ) ) ;
#462=CARTESIAN_POINT ( 'NONE',  ( 0.000000000000000000, 0.000000000000000000, 0.000000000000000000 ) ) ;
#463=CIRCLE ( 'NONE', #817, 2.041999999999999815 ) ;
#466=PRODUCT ( 'socket head cap screw_iso_ISO 4762 M5 x 20 - 20N', 'socket head cap screw_iso_ISO 4762 M5 x 20 - 20N', '', ( #3718 ) ) ;
#478=DIRECTION ( 'NONE',  ( 0.000000000000000000, 0.000000000000000000, -1.000000000000000000 ) ) ;
#487=CARTESIAN_POINT ( 'NONE',  ( -31.74999999999995737, 0.000000000000000000, 0.000000000000000000 ) ) ;
#494=SURFACE_STYLE_USAGE ( .BOTH. , #3060 ) ;
#512=LINE ( 'NONE', #2245, #1941 ) ;
#514=DIRECTION ( 'NONE',  ( 0.000000000000000000, 0.5000000000000011102, 0.8660254037844380415 ) ) ;
#516=VERTEX_POINT ( 'NONE', #9391 ) ;
#521=CARTESIAN_POINT ( 'NONE',  ( 25.00000000000000000, 0.000000000000000000, 0.000000000000000000 ) ) ;
#530=APPLICATION_CONTEXT ( 'automotive_design' ) ;
#547=VECTOR ( 'NONE', #5638, 1000.000000000000114 ) ;
#552=EDGE_LOOP ( 'NONE', ( #3265, #5644 ) ) ;
#559=LINE ( 'NONE', #7512, #10322 ) ;
#570=LINE ( 'NONE', #9920, #2381 ) ;
#591=AXIS2_PLACEMENT_3D ( 'NONE', #4501, #3714, #7053 ) ;
#600=VECTOR ( 'NONE', #4787, 1000.000000000000000 ) ;
#614=CONICAL_SURFACE ( 'NONE', #2233, 2.055000000000000160, 0.7853981633974721488 ) ;
#625=VERTEX_POINT ( 'NONE', #5340 ) ;
#637=DIRECTION ( 'NONE',  ( -1.000000000000000000, -0.000000000000000000, -0.000000000000000000 ) ) ;
#638=VECTOR ( 'NONE', #3810, 1000.000000000000000 ) ;
#647=VERTEX_POINT ( 'NONE', #7310 ) ;
#650=EDGE_LOOP ( 'NONE', ( #9124, #3568, #718, #1775 ) ) ;
#655=ORIENTED_EDGE ( 'NONE', *, *, #2585, .T. ) ;
#668=VECTOR ( 'NONE', #8809, 1000.000000000000114 ) ;
#673=DIRECTION ( 'NONE',  ( 0.000000000000000000, 0.000000000000000000, -1.000000000000000000 ) ) ;
#718=ORIENTED_EDGE ( 'NONE', *, *, #9054, .T. ) ;
#749=EDGE_CURVE ( 'NONE', #8234, #5182, #5392, .T. ) ;
#751=ORIENTED_EDGE ( 'NONE', *, *, #7672, .T. ) ;
#766=ORIENTED_EDGE ( 'NONE', *, *, #8949, .T. ) ;
#771=ADVANCED_FACE ( 'NONE', ( #9607 ), #4510, .F. ) ;
#772=EDGE_CURVE ( 'NONE', #647, #318, #5378, .T. ) ;
#787=DIRECTION ( 'NONE',  ( 0.000000000000000000, 0.000000000000000000, -1.000000000000000000 ) ) ;
#794=CARTESIAN_POINT ( 'NONE',  ( 0.2500000000000002220, 0.000000000000000000, 0.000000000000000000 ) ) ;
#797=DIRECTION ( 'NONE',  ( 1.000000000000000000, 0.000000000000000000, 0.000000000000000000 ) ) ;
#810=ORIENTED_EDGE ( 'NONE', *, *, #5380, .F. ) ;
#817=AXIS2_PLACEMENT_3D ( 'NONE', #4988, #5159, #5980 ) ;
#849=ORIENTED_EDGE ( 'NONE', *, *, #4961, .F. ) ;
#854=PLANE ( 'NONE',  #9315 ) ;
#855=STYLED_ITEM ( 'NONE', ( #9750 ), #1910 ) ;
#869=CARTESIAN_POINT ( 'NONE',  ( 2.500000000000000000, 1.178949249685218525, 2.041999999999999371 ) ) ;
#894=( NAMED_UNIT ( * ) PLANE_ANGLE_UNIT ( ) SI_UNIT ( $, .RADIAN. ) );
#979=ADVANCED_FACE ( 'NONE', ( #1837 ), #5230, .T. ) ;
#1000=AXIS2_PLACEMENT_3D ( 'NONE', #2081, #3534, #1071 ) ;
#1014=ORIENTED_EDGE ( 'NONE', *, *, #7639, .T. ) ;
#1028=AXIS2_PLACEMENT_3D ( 'NONE', #5558, #8939, #7269 ) ;
#1052=CARTESIAN_POINT ( 'NONE',  ( 0.000000000000000000, -1.178949249685213863, 2.042000000000002924 ) ) ;
#1063=PLANE ( 'NONE',  #7417 ) ;
#1071=DIRECTION ( 'NONE',  ( 0.000000000000000000, 0.000000000000000000, -1.000000000000000000 ) ) ;
#1097=EDGE_LOOP ( 'NONE', ( #5766, #2854, #1150 ) ) ;
#1101=ADVANCED_FACE ( 'NONE', ( #4326 ), #7142, .F. ) ;
#1126=CARTESIAN_POINT ( 'NONE',  ( 5.000000000000000888, 0.000000000000000000, 0.000000000000000000 ) ) ;
#1127=CARTESIAN_POINT ( 'NONE',  ( 2.500000000000000000, 2.357898499370433054, -1.951563910473907981E-15 ) ) ;
#1135=DIRECTION ( 'NONE',  ( 0.000000000000000000, 0.000000000000000000, 1.000000000000000000 ) ) ;
#1150=ORIENTED_EDGE ( 'NONE', *, *, #7639, .F. ) ;
#1168=VERTEX_POINT ( 'NONE', #5983 ) ;
#1186=ORIENTED_EDGE ( 'NONE', *, *, #1270, .F. ) ;
#1240=EDGE_CURVE ( 'NONE', #2458, #625, #4211, .T. ) ;
#1270=EDGE_CURVE ( 'NONE', #5182, #8762, #6040, .T. ) ;
#1274=ORIENTED_EDGE ( 'NONE', *, *, #5530, .F. ) ;
#1282=DIRECTION ( 'NONE',  ( -1.000000000000000000, -0.000000000000000000, -0.000000000000000000 ) ) ;
#1303=( NAMED_UNIT ( * ) PLANE_ANGLE_UNIT ( ) SI_UNIT ( $, .RADIAN. ) );
#1394=CIRCLE ( 'NONE', #1028, 0.2000000000000000944 ) ;
#1396=( NAMED_UNIT ( * ) PLANE_ANGLE_UNIT ( ) SI_UNIT ( $, .RADIAN. ) );
#1410=PLANE ( 'NONE',  #7732 ) ;
#1416=ADVANCED_FACE ( 'NONE', ( #2154 ), #1999, .F. ) ;
#1443=FILL_AREA_STYLE ('',( #6436 ) ) ;
#1480=CARTESIAN_POINT ( 'NONE',  ( 5.000000000000000888, 4.250000000000000000, 0.000000000000000000 ) ) ;
#1508=VERTEX_POINT ( 'NONE', #4029 ) ;
#1518=EDGE_LOOP ( 'NONE', ( #2852, #7234, #3175, #5621, #9061 ) ) ;
#1525=AXIS2_PLACEMENT_3D ( 'NONE', #8463, #2517, #9914 ) ;
#1536=CARTESIAN_POINT ( 'NONE',  ( 2.500000000000000000, 1.178949249685213863, -2.042000000000001148 ) ) ;
#1548=ORIENTED_EDGE ( 'NONE', *, *, #6325, .T. ) ;
#1559=CIRCLE ( 'NONE', #7784, 2.041999999999999815 ) ;
#1570=CARTESIAN_POINT ( 'NONE',  ( 2.500000000000000000, 1.178949249685213863, -2.042000000000001148 ) ) ;
#1579=DIRECTION ( 'NONE',  ( 0.000000000000000000, 0.000000000000000000, 1.000000000000000000 ) ) ;
#1588=DIRECTION ( 'NONE',  ( -1.000000000000000000, -0.000000000000000000, -0.000000000000000000 ) ) ;
#1602=ORIENTED_EDGE ( 'NONE', *, *, #7636, .T. ) ;
#1618=LINE ( 'NONE', #4347, #4412 ) ;
#1621=ORIENTED_EDGE ( 'NONE', *, *, #2893, .F. ) ;
#1654=EDGE_CURVE ( 'NONE', #10106, #7739, #2707, .T. ) ;
#1665=CARTESIAN_POINT ( 'NONE',  ( 25.00000000000000000, 0.000000000000000000, 0.000000000000000000 ) ) ;
#1677=AXIS2_PLACEMENT_3D ( 'NONE', #4954, #10878, #3266 ) ;
#1697=DIRECTION ( 'NONE',  ( 1.000000000000000000, 0.000000000000000000, 0.000000000000000000 ) ) ;
#1714=ORIENTED_EDGE ( 'NONE', *, *, #749, .F. ) ;
#1732=ORIENTED_EDGE ( 'NONE', *, *, #2433, .T. ) ;
#1761=DIRECTION ( 'NONE',  ( 0.000000000000000000, -0.5000000000000012212, -0.8660254037844380415 ) ) ;
#1774=EDGE_LOOP ( 'NONE', ( #3839, #9318, #3581, #10119, #9490, #6576 ) ) ;
#1775=ORIENTED_EDGE ( 'NONE', *, *, #5684, .F. ) ;
#1792=ORIENTED_EDGE ( 'NONE', *, *, #4130, .F. ) ;
#1828=CARTESIAN_POINT ( 'NONE',  ( 2.500000000000000000, -1.178949249685213863, 2.042000000000002924 ) ) ;
#1837=FACE_OUTER_BOUND ( 'NONE', #2647, .T. ) ;
#1853=EDGE_CURVE ( 'NONE', #7739, #625, #9635, .T. ) ;
#1861=CLOSED_SHELL ( 'NONE', ( #6431, #3852, #7424, #5521, #979, #7108, #8371, #10145, #9876, #9253, #7257, #3375, #1101, #9150, #3232, #771, #3744, #9256, #7361, #5940, #5339, #8158, #10303, #3290, #4867, #4724, #1416 ) ) ;
#1866=PLANE ( 'NONE',  #3983 ) ;
#1870=AXIS2_PLACEMENT_3D ( 'NONE', #8610, #7727, #1895 ) ;
#1895=DIRECTION ( 'NONE',  ( 0.000000000000000000, -0.4999999999999992784, 0.8660254037844389297 ) ) ;
#1910=MANIFOLD_SOLID_BREP ( 'Hex', #1861 ) ;
#1921=AXIS2_PLACEMENT_3D ( 'NONE', #5520, #8065, #8955 ) ;
#1940=EDGE_CURVE ( 'NONE', #7929, #8762, #512, .T. ) ;
#1941=VECTOR ( 'NONE', #456, 1000.000000000000000 ) ;
#1953=PLANE ( 'NONE',  #1870 ) ;
#1968=DIRECTION ( 'NONE',  ( 0.000000000000000000, 0.000000000000000000, -1.000000000000000000 ) ) ;
#1999=CONICAL_SURFACE ( 'NONE', #3944, 2.041999999999999815, 1.047197551196591858 ) ;
#2021=PLANE ( 'NONE',  #1000 ) ;
#2027=CARTESIAN_POINT ( 'NONE',  ( 0.000000000000000000, 2.357898499370433054, -1.951563910473907981E-15 ) ) ;
#2061=VERTEX_POINT ( 'NONE', #8182 ) ;
#2065=TOROIDAL_SURFACE ( 'NONE', #1525, 4.000000000000000000, 0.2500000000000000000 ) ;
#2081=CARTESIAN_POINT ( 'NONE',  ( 2.500000000000000000, 2.357898499370433054, -1.951563910473907981E-15 ) ) ;
#2083=LINE ( 'NONE', #9524, #8086 ) ;
#2109=DIRECTION ( 'NONE',  ( 0.000000000000000000, 0.000000000000000000, -1.000000000000000000 ) ) ;
#2122=LINE ( 'NONE', #7898, #9725 ) ;
#2131=CARTESIAN_POINT ( 'NONE',  ( 2.500000000000000000, -1.768423874527823791, -1.020999999999998353 ) ) ;
#2154=FACE_OUTER_BOUND ( 'NONE', #9138, .T. ) ;
#2155=PLANE ( 'NONE',  #94 ) ;
#2158=FACE_OUTER_BOUND ( 'NONE', #10771, .T. ) ;
#2161=CARTESIAN_POINT ( 'NONE',  ( 2.500000000000000000, 1.178949249685213863, -2.042000000000001148 ) ) ;
#2166=DIRECTION ( 'NONE',  ( 0.000000000000000000, 0.000000000000000000, 1.000000000000000000 ) ) ;
#2168=ORIENTED_EDGE ( 'NONE', *, *, #6266, .F. ) ;
#2195=CARTESIAN_POINT ( 'NONE',  ( 0.000000000000000000, 0.000000000000000000, 0.000000000000000000 ) ) ;
#2206=PLANE ( 'NONE',  #2741 ) ;
#2213=AXIS2_PLACEMENT_3D ( 'NONE', #5591, #4709, #8244 ) ;
#2222=VERTEX_POINT ( 'NONE', #5788 ) ;
#2233=AXIS2_PLACEMENT_3D ( 'NONE', #521, #4927, #5650 ) ;
#2245=CARTESIAN_POINT ( 'NONE',  ( 0.000000000000000000, 1.178949249685213863, -2.042000000000001148 ) ) ;
#2276=EDGE_CURVE ( 'NONE', #7380, #7929, #9174, .T. ) ;
#2282=( GEOMETRIC_REPRESENTATION_CONTEXT ( 3 ) GLOBAL_UNCERTAINTY_ASSIGNED_CONTEXT ( ( #7877 ) ) GLOBAL_UNIT_ASSIGNED_CONTEXT ( ( #7329, #894, #9891 ) ) REPRESENTATION_CONTEXT ( 'NONE', 'WORKASPACE' ) );
#2312=FACE_OUTER_BOUND ( 'NONE', #7167, .T. ) ;
#2315=PLANE ( 'NONE',  #9113 ) ;
#2343=CARTESIAN_POINT ( 'NONE',  ( 2.500000000000000000, 2.357898499370433054, -1.951563910473907981E-15 ) ) ;
#2358=DIRECTION ( 'NONE',  ( -1.000000000000000000, -0.000000000000000000, -0.000000000000000000 ) ) ;
#2373=TOROIDAL_SURFACE ( 'NONE', #6995, 2.700000000000001066, 0.2000000000000000111 ) ;
#2381=VECTOR ( 'NONE', #7355, 999.9999999999998863 ) ;
#2394=VECTOR ( 'NONE', #10448, 1000.000000000000000 ) ;
#2409=EDGE_CURVE ( 'NONE', #4976, #7117, #5094, .T. ) ;
#2433=EDGE_CURVE ( 'NONE', #3779, #3173, #8544, .T. ) ;
#2458=VERTEX_POINT ( 'NONE', #9922 ) ;
#2480=EDGE_CURVE ( 'NONE', #2061, #7117, #9781, .T. ) ;
#2483=EDGE_LOOP ( 'NONE', ( #6153, #4477, #810 ) ) ;
#2491=ORIENTED_EDGE ( 'NONE', *, *, #772, .F. ) ;
#2495=CARTESIAN_POINT ( 'NONE',  ( 2.500000000000000000, -1.178949249685213863, 2.042000000000002924 ) ) ;
#2499=DIRECTION ( 'NONE',  ( 0.000000000000000000, 0.000000000000000000, 1.000000000000000000 ) ) ;
#2517=DIRECTION ( 'NONE',  ( -1.000000000000000000, -0.000000000000000000, -0.000000000000000000 ) ) ;
#2550=EDGE_CURVE ( 'NONE', #8234, #625, #7816, .T. ) ;
#2578=CIRCLE ( 'NONE', #2213, 2.041999999999999815 ) ;
#2585=EDGE_CURVE ( 'NONE', #6989, #2222, #21, .T. ) ;
#2587=CARTESIAN_POINT ( 'NONE',  ( 0.2500000000000002220, 0.000000000000000000, 0.000000000000000000 ) ) ;
#2589=FACE_OUTER_BOUND ( 'NONE', #2483, .T. ) ;
#2592=AXIS2_PLACEMENT_3D ( 'NONE', #8307, #797, #10920 ) ;
#2594=CARTESIAN_POINT ( 'NONE',  ( 2.500000000000000000, 2.357898499370433054, -1.951563910473907981E-15 ) ) ;
#2645=DIRECTION ( 'NONE',  ( 0.000000000000000000, 0.5000000000000012212, 0.8660254037844380415 ) ) ;
#2647=EDGE_LOOP ( 'NONE', ( #7608, #2672, #6760, #3825 ) ) ;
#2648=CIRCLE ( 'NONE', #6900, 2.041999999999999815 ) ;
#2653=DIRECTION ( 'NONE',  ( 0.000000000000000000, -1.224646799147353454E-16, 1.000000000000000000 ) ) ;
#2657=DIRECTION ( 'NONE',  ( 1.000000000000000000, 0.000000000000000000, 0.000000000000000000 ) ) ;
#2662=DIRECTION ( 'NONE',  ( -0.7071067811865306973, 8.659560562355138702E-17, -0.7071067811865643371 ) ) ;
#2664=LINE ( 'NONE', #7771, #4542 ) ;
#2672=ORIENTED_EDGE ( 'NONE', *, *, #2952, .T. ) ;
#2675=FACE_OUTER_BOUND ( 'NONE', #4152, .T. ) ;
#2676=EDGE_CURVE ( 'NONE', #10106, #5275, #6133, .T. ) ;
#2707=LINE ( 'NONE', #7759, #6892 ) ;
#2730=DIRECTION ( 'NONE',  ( 0.000000000000000000, 0.000000000000000000, 1.000000000000000000 ) ) ;
#2734=DIRECTION ( 'NONE',  ( -0.5000000000000051070, 1.060575238724903217E-16, -0.8660254037844355990 ) ) ;
#2741=AXIS2_PLACEMENT_3D ( 'NONE', #1480, #4876, #478 ) ;
#2759=AXIS2_PLACEMENT_3D ( 'NONE', #6047, #4281, #4224 ) ;
#2765=AXIS2_PLACEMENT_3D ( 'NONE', #6720, #4694, #2499 ) ;
#2772=EDGE_CURVE ( 'NONE', #10106, #1168, #9798, .T. ) ;
#2795=ORIENTED_EDGE ( 'NONE', *, *, #6811, .F. ) ;
#2813=CIRCLE ( 'NONE', #1921, 2.500000000000001332 ) ;
#2834=DIRECTION ( 'NONE',  ( -1.000000000000000000, -0.000000000000000000, -0.000000000000000000 ) ) ;
#2850=ORIENTED_EDGE ( 'NONE', *, *, #9742, .T. ) ;
#2852=ORIENTED_EDGE ( 'NONE', *, *, #10099, .F. ) ;
#2854=ORIENTED_EDGE ( 'NONE', *, *, #2676, .T. ) ;
#2860=DIRECTION ( 'NONE',  ( -1.000000000000000000, -0.000000000000000000, -0.000000000000000000 ) ) ;
#2881=DIRECTION ( 'NONE',  ( -1.000000000000000000, -0.000000000000000000, -0.000000000000000000 ) ) ;
#2893=EDGE_CURVE ( 'NONE', #3442, #3173, #8183, .T. ) ;
#2929=VERTEX_POINT ( 'NONE', #5689 ) ;
#2940=FACE_OUTER_BOUND ( 'NONE', #3397, .T. ) ;
#2952=EDGE_CURVE ( 'NONE', #4616, #2061, #559, .T. ) ;
#2979=DIRECTION ( 'NONE',  ( 1.000000000000000000, 0.000000000000000000, 0.000000000000000000 ) ) ;
#3060=SURFACE_SIDE_STYLE ('',( #3891 ) ) ;
#3111=CARTESIAN_POINT ( 'NONE',  ( 2.500000000000000000, 0.000000000000000000, 0.000000000000000000 ) ) ;
#3121=DIRECTION ( 'NONE',  ( -1.000000000000000000, -0.000000000000000000, -0.000000000000000000 ) ) ;
#3133=ORIENTED_EDGE ( 'NONE', *, *, #9054, .F. ) ;
#3139=CARTESIAN_POINT ( 'NONE',  ( -31.74999999999995737, 0.000000000000000000, 2.500000000000000888 ) ) ;
#3155=EDGE_LOOP ( 'NONE', ( #1792, #9989 ) ) ;
#3173=VERTEX_POINT ( 'NONE', #8198 ) ;
#3175=ORIENTED_EDGE ( 'NONE', *, *, #772, .T. ) ;
#3181=CARTESIAN_POINT ( 'NONE',  ( -31.74999999999995737, 0.000000000000000000, 4.250000000000000000 ) ) ;
#3191=DIRECTION ( 'NONE',  ( 1.000000000000000000, 0.000000000000000000, 0.000000000000000000 ) ) ;
#3198=EDGE_CURVE ( 'NONE', #4891, #7578, #10742, .T. ) ;
#3212=DIRECTION ( 'NONE',  ( 0.000000000000000000, 0.000000000000000000, 1.000000000000000000 ) ) ;
#3232=ADVANCED_FACE ( 'NONE', ( #2940 ), #2155, .T. ) ;
#3249=DIRECTION ( 'NONE',  ( 0.000000000000000000, 0.000000000000000000, -1.000000000000000000 ) ) ;
#3265=ORIENTED_EDGE ( 'NONE', *, *, #8857, .T. ) ;
#3266=DIRECTION ( 'NONE',  ( 0.000000000000000000, 0.000000000000000000, 1.000000000000000000 ) ) ;
#3277=FILL_AREA_STYLE_COLOUR ( '', #3876 ) ;
#3279=CIRCLE ( 'NONE', #3818, 2.055000000000000160 ) ;
#3290=ADVANCED_FACE ( 'NONE', ( #2312 ), #10809, .F. ) ;
#3292=VECTOR ( 'NONE', #347, 1000.000000000000000 ) ;
#3296=DIRECTION ( 'NONE',  ( -1.000000000000000000, -0.000000000000000000, -0.000000000000000000 ) ) ;
#3323=ORIENTED_EDGE ( 'NONE', *, *, #3198, .T. ) ;
#3325=CARTESIAN_POINT ( 'NONE',  ( 5.000000000000002665, 0.000000000000000000, -2.700000000000001066 ) ) ;
#3337=SURFACE_STYLE_USAGE ( .BOTH. , #5531 ) ;
#3371=EDGE_CURVE ( 'NONE', #3819, #6902, #7738, .T. ) ;
#3375=ADVANCED_FACE ( 'NONE', ( #4985 ), #7592, .T. ) ;
#3378=DIRECTION ( 'NONE',  ( -1.000000000000000000, -0.000000000000000000, -0.000000000000000000 ) ) ;
#3397=EDGE_LOOP ( 'NONE', ( #370, #8416, #9099, #3517, #3439 ) ) ;
#3398=DIRECTION ( 'NONE',  ( -1.000000000000000000, -0.000000000000000000, -0.000000000000000000 ) ) ;
#3427=CARTESIAN_POINT ( 'NONE',  ( 2.500000000000000000, 2.357898499370433054, -1.951563910473907981E-15 ) ) ;
#3439=ORIENTED_EDGE ( 'NONE', *, *, #1240, .T. ) ;
#3442=VERTEX_POINT ( 'NONE', #6084 ) ;
#3449=DIRECTION ( 'NONE',  ( -1.000000000000000000, -0.000000000000000000, -0.000000000000000000 ) ) ;
#3480=CARTESIAN_POINT ( 'NONE',  ( 0.2500000000000002220, 4.898587196589412829E-16, -4.000000000000000000 ) ) ;
#3481=DIRECTION ( 'NONE',  ( 0.000000000000000000, 1.000000000000000000, -1.471414886128461471E-15 ) ) ;
#3488=LINE ( 'NONE', #6870, #151 ) ;
#3517=ORIENTED_EDGE ( 'NONE', *, *, #5228, .T. ) ;
#3534=DIRECTION ( 'NONE',  ( 1.000000000000000000, 0.000000000000000000, 0.000000000000000000 ) ) ;
#3540=DIRECTION ( 'NONE',  ( -1.000000000000000000, -0.000000000000000000, -0.000000000000000000 ) ) ;
#3541=DIRECTION ( 'NONE',  ( 0.000000000000000000, 0.000000000000000000, -1.000000000000000000 ) ) ;
#3546=CARTESIAN_POINT ( 'NONE',  ( 0.000000000000000000, -2.357898499370432610, 3.252606517456513302E-15 ) ) ;
#3554=CARTESIAN_POINT ( 'NONE',  ( 5.200000000000002842, 0.000000000000000000, 0.000000000000000000 ) ) ;
#3555=LINE ( 'NONE', #2495, #5411 ) ;
#3568=ORIENTED_EDGE ( 'NONE', *, *, #4103, .F. ) ;
#3576=VECTOR ( 'NONE', #2358, 1000.000000000000000 ) ;
#3577=CARTESIAN_POINT ( 'NONE',  ( 2.500000000000000000, 2.357898499370433054, -1.951563910473907981E-15 ) ) ;
#3581=ORIENTED_EDGE ( 'NONE', *, *, #749, .T. ) ;
#3654=AXIS2_PLACEMENT_3D ( 'NONE', #7924, #2979, #6354 ) ;
#3660=CARTESIAN_POINT ( 'NONE',  ( 0.000000000000000000, 5.051668046482832750E-16, -4.000000000000000000 ) ) ;
#3663=ORIENTED_EDGE ( 'NONE', *, *, #8236, .T. ) ;
#3671=DIRECTION ( 'NONE',  ( -1.000000000000000000, -0.000000000000000000, -0.000000000000000000 ) ) ;
#3699=ORIENTED_EDGE ( 'NONE', *, *, #3371, .F. ) ;
#3714=DIRECTION ( 'NONE',  ( -1.000000000000000000, -0.000000000000000000, -0.000000000000000000 ) ) ;
#3718=PRODUCT_CONTEXT ( 'NONE', #530, 'mechanical' ) ;
#3740=ORIENTED_EDGE ( 'NONE', *, *, #8808, .F. ) ;
#3743=DIRECTION ( 'NONE',  ( 0.000000000000000000, 0.000000000000000000, -1.000000000000000000 ) ) ;
#3744=ADVANCED_FACE ( 'NONE', ( #6300 ), #8137, .T. ) ;
#3767=DIRECTION ( 'NONE',  ( 0.000000000000000000, 0.000000000000000000, 1.000000000000000000 ) ) ;
#3779=VERTEX_POINT ( 'NONE', #8400 ) ;
#3803=DIRECTION ( 'NONE',  ( 0.000000000000000000, 0.8660254037844380415, -0.5000000000000011102 ) ) ;
#3810=DIRECTION ( 'NONE',  ( 0.000000000000000000, 0.4999999999999993339, -0.8660254037844390407 ) ) ;
#3818=AXIS2_PLACEMENT_3D ( 'NONE', #1665, #5063, #5526 ) ;
#3819=VERTEX_POINT ( 'NONE', #7403 ) ;
#3825=ORIENTED_EDGE ( 'NONE', *, *, #2409, .F. ) ;
#3826=LINE ( 'NONE', #2161, #2394 ) ;
#3839=ORIENTED_EDGE ( 'NONE', *, *, #1853, .T. ) ;
#3852=ADVANCED_FACE ( 'NONE', ( #9178 ), #2065, .T. ) ;
#3869=DIRECTION ( 'NONE',  ( 0.000000000000000000, 0.000000000000000000, 1.000000000000000000 ) ) ;
#3876=COLOUR_RGB ( '', 0.31764706, 0.68627451, 0.89019608) ;
#3887=EDGE_LOOP ( 'NONE', ( #9823, #655, #4584 ) ) ;
#3891=SURFACE_STYLE_FILL_AREA ( #1443 ) ;
#3911=SURFACE_STYLE_FILL_AREA ( #5837 ) ;
#3944=AXIS2_PLACEMENT_3D ( 'NONE', #9541, #2834, #6316 ) ;
#3948=AXIS2_PLACEMENT_3D ( 'NONE', #6167, #8726, #7896 ) ;
#3950=LINE ( 'NONE', #6602, #9899 ) ;
#3951=ORIENTED_EDGE ( 'NONE', *, *, #2893, .T. ) ;
#3983=AXIS2_PLACEMENT_3D ( 'NONE', #3427, #2657, #3541 ) ;
#4029=CARTESIAN_POINT ( 'NONE',  ( 2.500000000000000000, -1.178949249685218303, -2.041999999999998039 ) ) ;
#4031=ORIENTED_EDGE ( 'NONE', *, *, #2433, .F. ) ;
#4038=EDGE_CURVE ( 'NONE', #4616, #4976, #4379, .T. ) ;
#4053=AXIS2_PLACEMENT_3D ( 'NONE', #487, #9775, #2166 ) ;
#4080=DIRECTION ( 'NONE',  ( -1.000000000000000000, -0.000000000000000000, -0.000000000000000000 ) ) ;
#4103=EDGE_CURVE ( 'NONE', #3173, #3779, #10582, .T. ) ;
#4123=AXIS2_PLACEMENT_3D ( 'NONE', #275, #3671, #7063 ) ;
#4130=EDGE_CURVE ( 'NONE', #3442, #9151, #5264, .T. ) ;
#4141=CARTESIAN_POINT ( 'NONE',  ( 5.200000000000002842, 0.000000000000000000, 0.000000000000000000 ) ) ;
#4148=ORIENTED_EDGE ( 'NONE', *, *, #7636, .F. ) ;
#4152=EDGE_LOOP ( 'NONE', ( #1186, #8455, #6538, #7128, #4716 ) ) ;
#4154=ORIENTED_EDGE ( 'NONE', *, *, #6598, .T. ) ;
#4211=LINE ( 'NONE', #869, #4840 ) ;
#4224=DIRECTION ( 'NONE',  ( 0.000000000000000000, 0.000000000000000000, -1.000000000000000000 ) ) ;
#4281=DIRECTION ( 'NONE',  ( 0.000000000000000000, -1.000000000000000000, 0.000000000000000000 ) ) ;
#4296=DIRECTION ( 'NONE',  ( 0.000000000000000000, 0.000000000000000000, 1.000000000000000000 ) ) ;
#4326=FACE_OUTER_BOUND ( 'NONE', #6387, .T. ) ;
#4329=ORIENTED_EDGE ( 'NONE', *, *, #8859, .T. ) ;
#4347=CARTESIAN_POINT ( 'NONE',  ( 2.500000000000000000, 2.500728763858895382E-16, -2.041999999999999815 ) ) ;
#4359=LINE ( 'NONE', #3577, #10970 ) ;
#4372=DIRECTION ( 'NONE',  ( 0.000000000000000000, 1.000000000000000000, -1.471414886128461471E-15 ) ) ;
#4379=CIRCLE ( 'NONE', #6142, 2.500000000000001332 ) ;
#4388=CARTESIAN_POINT ( 'NONE',  ( 5.200000000000002842, 0.000000000000000000, 0.000000000000000000 ) ) ;
#4412=VECTOR ( 'NONE', #2734, 1000.000000000000114 ) ;
#4443=UNCERTAINTY_MEASURE_WITH_UNIT (LENGTH_MEASURE( 1.000000000000000082E-05 ), #9003, 'distance_accuracy_value', 'NONE');
#4465=EDGE_LOOP ( 'NONE', ( #4031, #7377, #5384, #3133 ) ) ;
#4473=VECTOR ( 'NONE', #1761, 999.9999999999998863 ) ;
#4474=CARTESIAN_POINT ( 'NONE',  ( 2.500000000000000000, 2.357898499370433054, -1.951563910473907981E-15 ) ) ;
#4477=ORIENTED_EDGE ( 'NONE', *, *, #8457, .T. ) ;
#4496=CARTESIAN_POINT ( 'NONE',  ( 0.000000000000000000, -2.357898499370432610, 3.252606517456513302E-15 ) ) ;
#4501=CARTESIAN_POINT ( 'NONE',  ( 25.00000000000000000, 0.000000000000000000, 0.000000000000000000 ) ) ;
#4506=EDGE_CURVE ( 'NONE', #6542, #318, #408, .T. ) ;
#4510=PLANE ( 'NONE',  #3948 ) ;
#4542=VECTOR ( 'NONE', #150, 1000.000000000000000 ) ;
#4558=LINE ( 'NONE', #6992, #6634 ) ;
#4559=ORIENTED_EDGE ( 'NONE', *, *, #9566, .T. ) ;
#4561=AXIS2_PLACEMENT_3D ( 'NONE', #5641, #3803, #514 ) ;
#4584=ORIENTED_EDGE ( 'NONE', *, *, #6745, .F. ) ;
#4599=DIRECTION ( 'NONE',  ( -1.000000000000000000, -0.000000000000000000, -0.000000000000000000 ) ) ;
#4607=CARTESIAN_POINT ( 'NONE',  ( 24.55500000000002103, 0.000000000000000000, 0.000000000000000000 ) ) ;
#4613=DIRECTION ( 'NONE',  ( 1.000000000000000000, 0.000000000000000000, 0.000000000000000000 ) ) ;
#4616=VERTEX_POINT ( 'NONE', #9969 ) ;
#4623=CARTESIAN_POINT ( 'NONE',  ( 2.500000000000000000, 0.000000000000000000, 0.000000000000000000 ) ) ;
#4657=DIRECTION ( 'NONE',  ( 0.000000000000000000, 0.000000000000000000, 1.000000000000000000 ) ) ;
#4694=DIRECTION ( 'NONE',  ( -1.000000000000000000, -0.000000000000000000, -0.000000000000000000 ) ) ;
#4698=( NAMED_UNIT ( * ) SI_UNIT ( $, .STERADIAN. ) SOLID_ANGLE_UNIT ( ) );
#4709=DIRECTION ( 'NONE',  ( -1.000000000000000000, -0.000000000000000000, -0.000000000000000000 ) ) ;
#4716=ORIENTED_EDGE ( 'NONE', *, *, #6266, .T. ) ;
#4720=CARTESIAN_POINT ( 'NONE',  ( 2.500000000000000000, 1.178949249685213863, -2.042000000000001148 ) ) ;
#4724=ADVANCED_FACE ( 'NONE', ( #2589 ), #854, .F. ) ;
#4754=AXIS2_PLACEMENT_3D ( 'NONE', #462, #4599, #1135 ) ;
#4756=CARTESIAN_POINT ( 'NONE',  ( 2.500000000000000000, 2.357898499370433054, -1.951563910473907981E-15 ) ) ;
#4767=CARTESIAN_POINT ( 'NONE',  ( 2.500000000000000000, -1.768423874527823569, 1.021000000000002794 ) ) ;
#4772=DIRECTION ( 'NONE',  ( -1.000000000000000000, -0.000000000000000000, -0.000000000000000000 ) ) ;
#4783=FACE_OUTER_BOUND ( 'NONE', #9355, .T. ) ;
#4787=DIRECTION ( 'NONE',  ( 0.000000000000000000, -1.000000000000000000, 1.287488025362403787E-15 ) ) ;
#4798=DIRECTION ( 'NONE',  ( -1.000000000000000000, -0.000000000000000000, -0.000000000000000000 ) ) ;
#4840=VECTOR ( 'NONE', #3378, 1000.000000000000000 ) ;
#4846=LINE ( 'NONE', #9845, #10608 ) ;
#4855=DIRECTION ( 'NONE',  ( -1.000000000000000000, -0.000000000000000000, -0.000000000000000000 ) ) ;
#4867=ADVANCED_FACE ( 'NONE', ( #9628 ), #2021, .F. ) ;
#4876=DIRECTION ( 'NONE',  ( 1.000000000000000000, 0.000000000000000000, 0.000000000000000000 ) ) ;
#4880=VECTOR ( 'NONE', #7097, 1000.000000000000114 ) ;
#4891=VERTEX_POINT ( 'NONE', #7864 ) ;
#4927=DIRECTION ( 'NONE',  ( -1.000000000000000000, -0.000000000000000000, -0.000000000000000000 ) ) ;
#4954=CARTESIAN_POINT ( 'NONE',  ( 5.000000000000004441, 0.000000000000000000, 0.000000000000000000 ) ) ;
#4961=EDGE_CURVE ( 'NONE', #318, #9904, #463, .T. ) ;
#4976=VERTEX_POINT ( 'NONE', #6633 ) ;
#4985=FACE_OUTER_BOUND ( 'NONE', #7211, .T. ) ;
#4988=CARTESIAN_POINT ( 'NONE',  ( 2.500000000000000000, 0.000000000000000000, 0.000000000000000000 ) ) ;
#4999=ORIENTED_EDGE ( 'NONE', *, *, #3198, .F. ) ;
#5053=CIRCLE ( 'NONE', #1677, 4.250000000000000000 ) ;
#5062=CIRCLE ( 'NONE', #257, 0.2500000000000002220 ) ;
#5063=DIRECTION ( 'NONE',  ( -1.000000000000000000, -0.000000000000000000, -0.000000000000000000 ) ) ;
#5094=LINE ( 'NONE', #3139, #3576 ) ;
#5100=ORIENTED_EDGE ( 'NONE', *, *, #10099, .T. ) ;
#5148=EDGE_CURVE ( 'NONE', #7578, #4616, #3488, .T. ) ;
#5159=DIRECTION ( 'NONE',  ( -1.000000000000000000, -0.000000000000000000, -0.000000000000000000 ) ) ;
#5172=CARTESIAN_POINT ( 'NONE',  ( 0.000000000000000000, -1.178949249685213863, 2.042000000000002924 ) ) ;
#5182=VERTEX_POINT ( 'NONE', #3546 ) ;
#5228=EDGE_CURVE ( 'NONE', #1168, #2458, #4359, .T. ) ;
#5230=CYLINDRICAL_SURFACE ( 'NONE', #211, 2.500000000000000888 ) ;
#5253=VECTOR ( 'NONE', #8922, 1000.000000000000000 ) ;
#5255=DIRECTION ( 'NONE',  ( 0.000000000000000000, -1.000000000000000000, 0.000000000000000000 ) ) ;
#5256=AXIS2_PLACEMENT_3D ( 'NONE', #10600, #4772, #3767 ) ;
#5264=CIRCLE ( 'NONE', #8802, 4.250000000000000000 ) ;
#5275=VERTEX_POINT ( 'NONE', #9514 ) ;
#5277=FACE_OUTER_BOUND ( 'NONE', #3155, .T. ) ;
#5339=ADVANCED_FACE ( 'NONE', ( #6282 ), #1063, .F. ) ;
#5340=CARTESIAN_POINT ( 'NONE',  ( 0.000000000000000000, 1.178949249685218525, 2.041999999999999371 ) ) ;
#5352=VECTOR ( 'NONE', #5902, 1000.000000000000000 ) ;
#5353=DIRECTION ( 'NONE',  ( 0.000000000000000000, 0.000000000000000000, 1.000000000000000000 ) ) ;
#5376=DIRECTION ( 'NONE',  ( 0.000000000000000000, 0.4999999999999993339, -0.8660254037844390407 ) ) ;
#5378=CIRCLE ( 'NONE', #4123, 2.041999999999999815 ) ;
#5380=EDGE_CURVE ( 'NONE', #5275, #647, #2648, .T. ) ;
#5384=ORIENTED_EDGE ( 'NONE', *, *, #8857, .F. ) ;
#5392=LINE ( 'NONE', #1052, #8743 ) ;
#5411=VECTOR ( 'NONE', #9266, 1000.000000000000114 ) ;
#5414=CARTESIAN_POINT ( 'NONE',  ( 0.2500000000000002220, 0.000000000000000000, 4.000000000000000000 ) ) ;
#5501=ORIENTED_EDGE ( 'NONE', *, *, #7851, .T. ) ;
#5520=CARTESIAN_POINT ( 'NONE',  ( 24.55500000000002103, 0.000000000000000000, 0.000000000000000000 ) ) ;
#5521=ADVANCED_FACE ( 'NONE', ( #4783 ), #10613, .T. ) ;
#5526=DIRECTION ( 'NONE',  ( 0.000000000000000000, 0.000000000000000000, 1.000000000000000000 ) ) ;
#5530=EDGE_CURVE ( 'NONE', #7117, #3819, #1394, .T. ) ;
#5531=SURFACE_SIDE_STYLE ('',( #3911 ) ) ;
#5540=LINE ( 'NONE', #7880, #5253 ) ;
#5558=CARTESIAN_POINT ( 'NONE',  ( 5.200000000000002842, 3.306546357697854719E-16, 2.700000000000001066 ) ) ;
#5591=CARTESIAN_POINT ( 'NONE',  ( 2.500000000000000000, 0.000000000000000000, 0.000000000000000000 ) ) ;
#5613=EDGE_LOOP ( 'NONE', ( #7626, #10268, #2850, #8380 ) ) ;
#5621=ORIENTED_EDGE ( 'NONE', *, *, #4961, .T. ) ;
#5638=DIRECTION ( 'NONE',  ( 0.000000000000000000, -0.4999999999999993894, 0.8660254037844389297 ) ) ;
#5641=CARTESIAN_POINT ( 'NONE',  ( 2.500000000000000000, -1.178949249685213863, 2.042000000000002924 ) ) ;
#5644=ORIENTED_EDGE ( 'NONE', *, *, #5684, .T. ) ;
#5650=DIRECTION ( 'NONE',  ( 0.000000000000000000, 0.000000000000000000, 1.000000000000000000 ) ) ;
#5654=STYLED_ITEM ( 'NONE', ( #9780 ), #9310 ) ;
#5684=EDGE_CURVE ( 'NONE', #7151, #516, #8115, .T. ) ;
#5689=CARTESIAN_POINT ( 'NONE',  ( 3.678949249685231848, 0.000000000000000000, 0.000000000000000000 ) ) ;
#5750=CIRCLE ( 'NONE', #10886, 2.500000000000000888 ) ;
#5757=SHAPE_REPRESENTATION ( 'socket head cap screw_iso_ISO 4762 M5 x 20 - 20N', ( #308 ), #2282 ) ;
#5766=ORIENTED_EDGE ( 'NONE', *, *, #2772, .F. ) ;
#5788=CARTESIAN_POINT ( 'NONE',  ( 2.500000000000000000, 3.004629197474318851E-15, 2.042000000000000259 ) ) ;
#5831=ORIENTED_EDGE ( 'NONE', *, *, #2952, .F. ) ;
#5837=FILL_AREA_STYLE ('',( #3277 ) ) ;
#5867=ORIENTED_EDGE ( 'NONE', *, *, #2480, .F. ) ;
#5879=EDGE_LOOP ( 'NONE', ( #3323, #10908, #8084, #7938 ) ) ;
#5886=CARTESIAN_POINT ( 'NONE',  ( 5.000000000000004441, 5.204748896376250699E-16, -4.250000000000000000 ) ) ;
#5902=DIRECTION ( 'NONE',  ( -1.000000000000000000, -0.000000000000000000, -0.000000000000000000 ) ) ;
#5911=DIRECTION ( 'NONE',  ( 0.000000000000000000, 0.000000000000000000, 1.000000000000000000 ) ) ;
#5940=ADVANCED_FACE ( 'NONE', ( #9459 ), #7808, .F. ) ;
#5954=AXIS2_PLACEMENT_3D ( 'NONE', #6696, #1588, #7472 ) ;
#5968=DIRECTION ( 'NONE',  ( 1.000000000000000000, 0.000000000000000000, 0.000000000000000000 ) ) ;
#5970=DIRECTION ( 'NONE',  ( 1.000000000000000000, 0.000000000000000000, 0.000000000000000000 ) ) ;
#5980=DIRECTION ( 'NONE',  ( 0.000000000000000000, 0.000000000000000000, 1.000000000000000000 ) ) ;
#5983=CARTESIAN_POINT ( 'NONE',  ( 2.500000000000000000, 1.768423874527824902, 1.020999999999999019 ) ) ;
#5987=ORIENTED_EDGE ( 'NONE', *, *, #6598, .F. ) ;
#6040=LINE ( 'NONE', #4496, #9439 ) ;
#6047=CARTESIAN_POINT ( 'NONE',  ( 5.200000000000002842, 0.000000000000000000, -2.700000000000001066 ) ) ;
#6048=AXIS2_PLACEMENT_3D ( 'NONE', #794, #3191, #10747 ) ;
#6061=ORIENTED_EDGE ( 'NONE', *, *, #7153, .T. ) ;
#6084=CARTESIAN_POINT ( 'NONE',  ( 5.000000000000004441, 0.000000000000000000, 4.250000000000000000 ) ) ;
#6123=CIRCLE ( 'NONE', #2759, 0.2000000000000000944 ) ;
#6133=LINE ( 'NONE', #2594, #4473 ) ;
#6142=AXIS2_PLACEMENT_3D ( 'NONE', #4607, #2881, #4657 ) ;
#6153=ORIENTED_EDGE ( 'NONE', *, *, #7918, .T. ) ;
#6167=CARTESIAN_POINT ( 'NONE',  ( 2.500000000000000000, -1.178949249685213863, 2.042000000000002924 ) ) ;
#6200=EDGE_CURVE ( 'NONE', #4976, #4616, #2813, .T. ) ;
#6215=CARTESIAN_POINT ( 'NONE',  ( 0.000000000000000000, 0.000000000000000000, 0.000000000000000000 ) ) ;
#6252=CARTESIAN_POINT ( 'NONE',  ( 2.500000000000000000, -1.178949249685213863, 2.042000000000002924 ) ) ;
#6266=EDGE_CURVE ( 'NONE', #1508, #8762, #4846, .T. ) ;
#6282=FACE_OUTER_BOUND ( 'NONE', #9073, .T. ) ;
#6300=FACE_OUTER_BOUND ( 'NONE', #8622, .T. ) ;
#6316=DIRECTION ( 'NONE',  ( 0.000000000000000000, 0.000000000000000000, 1.000000000000000000 ) ) ;
#6317=CARTESIAN_POINT ( 'NONE',  ( 2.500000000000000000, 2.357898499370433054, -1.951563910473907981E-15 ) ) ;
#6325=EDGE_CURVE ( 'NONE', #9151, #3779, #3950, .T. ) ;
#6342=CARTESIAN_POINT ( 'NONE',  ( 2.500000000000000000, 0.000000000000000000, 0.000000000000000000 ) ) ;
#6354=DIRECTION ( 'NONE',  ( 0.000000000000000000, 0.000000000000000000, -1.000000000000000000 ) ) ;
#6387=EDGE_LOOP ( 'NONE', ( #1274, #5867, #3663, #3699 ) ) ;
#6431=ADVANCED_FACE ( 'NONE', ( #10288 ), #6513, .F. ) ;
#6436=FILL_AREA_STYLE_COLOUR ( '', #6523 ) ;
#6487=DIRECTION ( 'NONE',  ( 0.000000000000000000, 0.4999999999999993339, -0.8660254037844390407 ) ) ;
#6489=DIRECTION ( 'NONE',  ( -1.000000000000000000, -0.000000000000000000, -0.000000000000000000 ) ) ;
#6494=EDGE_CURVE ( 'NONE', #2929, #647, #1618, .T. ) ;
#6513=CONICAL_SURFACE ( 'NONE', #10781, 2.041999999999999815, 1.047197551196591858 ) ;
#6523=COLOUR_RGB ( '', 0.31764706, 0.68627451, 0.89019608) ;
#6538=ORIENTED_EDGE ( 'NONE', *, *, #4506, .T. ) ;
#6542=VERTEX_POINT ( 'NONE', #10233 ) ;
#6550=FACE_OUTER_BOUND ( 'NONE', #650, .T. ) ;
#6576=ORIENTED_EDGE ( 'NONE', *, *, #8859, .F. ) ;
#6584=EDGE_LOOP ( 'NONE', ( #10785, #7734, #7115, #8634 ) ) ;
#6592=EDGE_LOOP ( 'NONE', ( #4999, #7392 ) ) ;
#6598=EDGE_CURVE ( 'NONE', #6989, #8234, #2122, .T. ) ;
#6602=CARTESIAN_POINT ( 'NONE',  ( -31.74999999999995737, 5.204748896376250699E-16, -4.250000000000000000 ) ) ;
#6633=CARTESIAN_POINT ( 'NONE',  ( 24.55500000000002103, 0.000000000000000000, 2.500000000000001332 ) ) ;
#6634=VECTOR ( 'NONE', #7832, 999.9999999999998863 ) ;
#6643=AXIS2_PLACEMENT_3D ( 'NONE', #6215, #7057, #7265 ) ;
#6664=ORIENTED_EDGE ( 'NONE', *, *, #1654, .T. ) ;
#6696=CARTESIAN_POINT ( 'NONE',  ( 5.000000000000000888, 0.000000000000000000, 0.000000000000000000 ) ) ;
#6720=CARTESIAN_POINT ( 'NONE',  ( 0.2500000000000002220, 0.000000000000000000, 0.000000000000000000 ) ) ;
#6728=ORIENTED_EDGE ( 'NONE', *, *, #5228, .F. ) ;
#6745=EDGE_CURVE ( 'NONE', #9904, #2222, #1559, .T. ) ;
#6757=AXIS2_PLACEMENT_3D ( 'NONE', #10859, #1697, #3249 ) ;
#6760=ORIENTED_EDGE ( 'NONE', *, *, #2480, .T. ) ;
#6771=DIRECTION ( 'NONE',  ( 0.000000000000000000, 0.000000000000000000, 1.000000000000000000 ) ) ;
#6809=CONICAL_SURFACE ( 'NONE', #591, 2.055000000000000160, 0.7853981633974721488 ) ;
#6811=EDGE_CURVE ( 'NONE', #318, #1508, #9000, .T. ) ;
#6814=AXIS2_PLACEMENT_3D ( 'NONE', #2195, #10649, #3869 ) ;
#6816=AXIS2_PLACEMENT_3D ( 'NONE', #3111, #6489, #3212 ) ;
#6860=DIRECTION ( 'NONE',  ( -0.000000000000000000, 1.000000000000000000, 1.224646799147353207E-16 ) ) ;
#6869=PRODUCT_DEFINITION_FORMATION_WITH_SPECIFIED_SOURCE ( 'ANY', '', #466, .NOT_KNOWN. ) ;
#6870=CARTESIAN_POINT ( 'NONE',  ( 25.00000000000000000, 2.516649172247811061E-16, -2.055000000000000160 ) ) ;
#6892=VECTOR ( 'NONE', #3540, 1000.000000000000000 ) ;
#6900=AXIS2_PLACEMENT_3D ( 'NONE', #6342, #2860, #5353 ) ;
#6902=VERTEX_POINT ( 'NONE', #3325 ) ;
#6956=CARTESIAN_POINT ( 'NONE',  ( 0.000000000000000000, 0.000000000000000000, 0.000000000000000000 ) ) ;
#6989=VERTEX_POINT ( 'NONE', #1828 ) ;
#6992=CARTESIAN_POINT ( 'NONE',  ( 2.500000000000000000, 2.357898499370433054, -1.951563910473907981E-15 ) ) ;
#6995=AXIS2_PLACEMENT_3D ( 'NONE', #4141, #7595, #10038 ) ;
#7033=CARTESIAN_POINT ( 'NONE',  ( 0.000000000000000000, -1.178949249685213863, 2.042000000000002924 ) ) ;
#7053=DIRECTION ( 'NONE',  ( 0.000000000000000000, 0.000000000000000000, 1.000000000000000000 ) ) ;
#7055=SHAPE_DEFINITION_REPRESENTATION ( #9791, #5757 ) ;
#7057=DIRECTION ( 'NONE',  ( -1.000000000000000000, 0.000000000000000000, -0.000000000000000000 ) ) ;
#7063=DIRECTION ( 'NONE',  ( 0.000000000000000000, 0.000000000000000000, 1.000000000000000000 ) ) ;
#7077=MECHANICAL_DESIGN_GEOMETRIC_PRESENTATION_REPRESENTATION('',(#855),#7420);
#7085=CARTESIAN_POINT ( 'NONE',  ( 2.500000000000000000, -1.178949249685213863, 2.042000000000002924 ) ) ;
#7097=DIRECTION ( 'NONE',  ( 0.000000000000000000, -0.5000000000000011102, -0.8660254037844379305 ) ) ;
#7108=ADVANCED_FACE ( 'NONE', ( #319 ), #6809, .T. ) ;
#7115=ORIENTED_EDGE ( 'NONE', *, *, #8949, .F. ) ;
#7117=VERTEX_POINT ( 'NONE', #7831 ) ;
#7128=ORIENTED_EDGE ( 'NONE', *, *, #6811, .T. ) ;
#7142=TOROIDAL_SURFACE ( 'NONE', #8201, 2.700000000000001066, 0.2000000000000000111 ) ;
#7151=VERTEX_POINT ( 'NONE', #3660 ) ;
#7153=EDGE_CURVE ( 'NONE', #7117, #2061, #5750, .T. ) ;
#7167=EDGE_LOOP ( 'NONE', ( #7543, #6728, #3740 ) ) ;
#7179=CIRCLE ( 'NONE', #6816, 2.041999999999999815 ) ;
#7183=TOROIDAL_SURFACE ( 'NONE', #2765, 4.000000000000000000, 0.2500000000000000000 ) ;
#7184=FACE_OUTER_BOUND ( 'NONE', #6592, .T. ) ;
#7194=ORIENTED_EDGE ( 'NONE', *, *, #2585, .F. ) ;
#7211=EDGE_LOOP ( 'NONE', ( #7382, #751, #3951, #330 ) ) ;
#7234=ORIENTED_EDGE ( 'NONE', *, *, #6494, .T. ) ;
#7257=ADVANCED_FACE ( 'NONE', ( #9487, #5277 ), #2206, .T. ) ;
#7265=DIRECTION ( 'NONE',  ( -0.000000000000000000, 0.000000000000000000, 1.000000000000000000 ) ) ;
#7269=DIRECTION ( 'NONE',  ( 0.000000000000000000, 1.224646799147353207E-16, 1.000000000000000000 ) ) ;
#7273=CARTESIAN_POINT ( 'NONE',  ( 25.00000000000000000, 2.789133085058098087E-16, -2.055000000000000160 ) ) ;
#7310=CARTESIAN_POINT ( 'NONE',  ( 2.500000000000000000, -2.629050547790028551E-15, -2.041999999999999815 ) ) ;
#7329=( LENGTH_UNIT ( ) NAMED_UNIT ( * ) SI_UNIT ( .MILLI., .METRE. ) );
#7343=CIRCLE ( 'NONE', #9843, 2.700000000000001066 ) ;
#7353=CIRCLE ( 'NONE', #6814, 4.000000000000000000 ) ;
#7355=DIRECTION ( 'NONE',  ( 0.000000000000000000, -0.5000000000000012212, -0.8660254037844380415 ) ) ;
#7361=ADVANCED_FACE ( 'NONE', ( #2158 ), #2315, .F. ) ;
#7374=AXIS2_PLACEMENT_3D ( 'NONE', #2587, #5968, #1579 ) ;
#7377=ORIENTED_EDGE ( 'NONE', *, *, #9972, .T. ) ;
#7380=VERTEX_POINT ( 'NONE', #1536 ) ;
#7382=ORIENTED_EDGE ( 'NONE', *, *, #6325, .F. ) ;
#7392=ORIENTED_EDGE ( 'NONE', *, *, #9182, .F. ) ;
#7403=CARTESIAN_POINT ( 'NONE',  ( 5.000000000000002665, 3.306546357697854226E-16, 2.700000000000001066 ) ) ;
#7417=AXIS2_PLACEMENT_3D ( 'NONE', #4474, #9680, #1968 ) ;
#7420=( GEOMETRIC_REPRESENTATION_CONTEXT ( 3 ) GLOBAL_UNCERTAINTY_ASSIGNED_CONTEXT ( ( #9859 ) ) GLOBAL_UNIT_ASSIGNED_CONTEXT ( ( #7500, #1303, #4698 ) ) REPRESENTATION_CONTEXT ( 'NONE', 'WORKASPACE' ) );
#7424=ADVANCED_FACE ( 'NONE', ( #10604 ), #2373, .F. ) ;
#7448=PRODUCT_DEFINITION_CONTEXT ( 'detailed design', #10477, 'design' ) ;
#7452=ORIENTED_EDGE ( 'NONE', *, *, #1240, .F. ) ;
#7472=DIRECTION ( 'NONE',  ( 0.000000000000000000, 0.000000000000000000, -1.000000000000000000 ) ) ;
#7500=( LENGTH_UNIT ( ) NAMED_UNIT ( * ) SI_UNIT ( .MILLI., .METRE. ) );
#7512=CARTESIAN_POINT ( 'NONE',  ( -31.74999999999995737, 3.061616997868384127E-16, -2.500000000000000888 ) ) ;
#7543=ORIENTED_EDGE ( 'NONE', *, *, #10008, .T. ) ;
#7578=VERTEX_POINT ( 'NONE', #7273 ) ;
#7592=CYLINDRICAL_SURFACE ( 'NONE', #9140, 4.250000000000000000 ) ;
#7595=DIRECTION ( 'NONE',  ( 1.000000000000000000, 0.000000000000000000, 0.000000000000000000 ) ) ;
#7608=ORIENTED_EDGE ( 'NONE', *, *, #6200, .T. ) ;
#7626=ORIENTED_EDGE ( 'NONE', *, *, #5148, .F. ) ;
#7636=EDGE_CURVE ( 'NONE', #647, #1508, #9833, .T. ) ;
#7639=EDGE_CURVE ( 'NONE', #1168, #5275, #7179, .T. ) ;
#7661=EDGE_LOOP ( 'NONE', ( #4329, #10827, #9448, #9282, #6664 ) ) ;
#7672=EDGE_CURVE ( 'NONE', #9151, #3442, #5053, .T. ) ;
#7727=DIRECTION ( 'NONE',  ( -0.000000000000000000, 0.8660254037844390407, 0.4999999999999993339 ) ) ;
#7732=AXIS2_PLACEMENT_3D ( 'NONE', #2343, #8285, #673 ) ;
#7734=ORIENTED_EDGE ( 'NONE', *, *, #5530, .T. ) ;
#7738=CIRCLE ( 'NONE', #5954, 2.700000000000001066 ) ;
#7739=VERTEX_POINT ( 'NONE', #10164 ) ;
#7748=DIRECTION ( 'NONE',  ( 0.000000000000000000, -0.4999999999999993894, 0.8660254037844389297 ) ) ;
#7759=CARTESIAN_POINT ( 'NONE',  ( 2.500000000000000000, 2.357898499370433054, -1.951563910473907981E-15 ) ) ;
#7771=CARTESIAN_POINT ( 'NONE',  ( 2.500000000000000000, -2.357898499370432610, 3.252606517456513302E-15 ) ) ;
#7773=DIRECTION ( 'NONE',  ( 0.000000000000000000, 0.000000000000000000, -1.000000000000000000 ) ) ;
#7784=AXIS2_PLACEMENT_3D ( 'NONE', #4623, #8008, #380 ) ;
#7808=PLANE ( 'NONE',  #9359 ) ;
#7816=LINE ( 'NONE', #7033, #7836 ) ;
#7831=CARTESIAN_POINT ( 'NONE',  ( 5.200000000000002842, 0.000000000000000000, 2.500000000000000888 ) ) ;
#7832=DIRECTION ( 'NONE',  ( 0.000000000000000000, -0.5000000000000012212, -0.8660254037844380415 ) ) ;
#7836=VECTOR ( 'NONE', #4372, 1000.000000000000000 ) ;
#7851=EDGE_CURVE ( 'NONE', #6989, #9904, #3555, .T. ) ;
#7864=CARTESIAN_POINT ( 'NONE',  ( 25.00000000000000000, 0.000000000000000000, 2.055000000000000160 ) ) ;
#7867=PLANE ( 'NONE',  #3654 ) ;
#7877=UNCERTAINTY_MEASURE_WITH_UNIT (LENGTH_MEASURE( 1.000000000000000082E-05 ), #7329, 'distance_accuracy_value', 'NONE');
#7880=CARTESIAN_POINT ( 'NONE',  ( 25.00000000000000000, 0.000000000000000000, 2.055000000000000160 ) ) ;
#7896=DIRECTION ( 'NONE',  ( 0.000000000000000000, -1.000000000000000000, 1.471414886128461471E-15 ) ) ;
#7898=CARTESIAN_POINT ( 'NONE',  ( 2.500000000000000000, -1.178949249685213863, 2.042000000000002924 ) ) ;
#7918=EDGE_CURVE ( 'NONE', #5275, #7380, #4558, .T. ) ;
#7924=CARTESIAN_POINT ( 'NONE',  ( 25.00000000000000000, 2.055000000000000160, 0.000000000000000000 ) ) ;
#7929=VERTEX_POINT ( 'NONE', #9595 ) ;
#7938=ORIENTED_EDGE ( 'NONE', *, *, #9742, .F. ) ;
#7939=( GEOMETRIC_REPRESENTATION_CONTEXT ( 3 ) GLOBAL_UNCERTAINTY_ASSIGNED_CONTEXT ( ( #4443 ) ) GLOBAL_UNIT_ASSIGNED_CONTEXT ( ( #9003, #1396, #9727 ) ) REPRESENTATION_CONTEXT ( 'NONE', 'WORKASPACE' ) );
#7954=ORIENTED_EDGE ( 'NONE', *, *, #4130, .T. ) ;
#7988=LINE ( 'NONE', #6252, #4880 ) ;
#8008=DIRECTION ( 'NONE',  ( -1.000000000000000000, -0.000000000000000000, -0.000000000000000000 ) ) ;
#8031=ORIENTED_EDGE ( 'NONE', *, *, #4506, .F. ) ;
#8037=CARTESIAN_POINT ( 'NONE',  ( 0.000000000000000000, -1.178949249685218303, -2.041999999999998039 ) ) ;
#8065=DIRECTION ( 'NONE',  ( -1.000000000000000000, -0.000000000000000000, -0.000000000000000000 ) ) ;
#8084=ORIENTED_EDGE ( 'NONE', *, *, #6200, .F. ) ;
#8086=VECTOR ( 'NONE', #8864, 1000.000000000000114 ) ;
#8115=CIRCLE ( 'NONE', #4754, 4.000000000000000000 ) ;
#8137=PLANE ( 'NONE',  #4561 ) ;
#8158=ADVANCED_FACE ( 'NONE', ( #8586 ), #1866, .F. ) ;
#8182=CARTESIAN_POINT ( 'NONE',  ( 5.200000000000002842, 3.061616997868384127E-16, -2.500000000000000888 ) ) ;
#8183=LINE ( 'NONE', #3181, #27 ) ;
#8198=CARTESIAN_POINT ( 'NONE',  ( 0.2500000000000002220, 0.000000000000000000, 4.250000000000000000 ) ) ;
#8201=AXIS2_PLACEMENT_3D ( 'NONE', #4388, #10323, #7773 ) ;
#8234=VERTEX_POINT ( 'NONE', #5172 ) ;
#8236=EDGE_CURVE ( 'NONE', #2061, #6902, #6123, .T. ) ;
#8244=DIRECTION ( 'NONE',  ( 0.000000000000000000, 0.000000000000000000, 1.000000000000000000 ) ) ;
#8285=DIRECTION ( 'NONE',  ( 1.000000000000000000, 0.000000000000000000, 0.000000000000000000 ) ) ;
#8307=CARTESIAN_POINT ( 'NONE',  ( 2.500000000000000000, 2.357898499370433054, -1.951563910473907981E-15 ) ) ;
#8371=ADVANCED_FACE ( 'NONE', ( #9771, #9657 ), #422, .T. ) ;
#8380=ORIENTED_EDGE ( 'NONE', *, *, #4038, .F. ) ;
#8400=CARTESIAN_POINT ( 'NONE',  ( 0.2500000000000002220, 5.204748896376250699E-16, -4.250000000000000000 ) ) ;
#8404=ORIENTED_EDGE ( 'NONE', *, *, #9617, .F. ) ;
#8416=ORIENTED_EDGE ( 'NONE', *, *, #1654, .F. ) ;
#8434=ORIENTED_EDGE ( 'NONE', *, *, #8808, .T. ) ;
#8455=ORIENTED_EDGE ( 'NONE', *, *, #9566, .F. ) ;
#8457=EDGE_CURVE ( 'NONE', #7380, #647, #3826, .T. ) ;
#8463=CARTESIAN_POINT ( 'NONE',  ( 0.2500000000000002220, 0.000000000000000000, 0.000000000000000000 ) ) ;
#8524=CARTESIAN_POINT ( 'NONE',  ( 2.500000000000000000, 2.357898499370433054, -1.951563910473907981E-15 ) ) ;
#8544=CIRCLE ( 'NONE', #6048, 4.250000000000000000 ) ;
#8560=EDGE_LOOP ( 'NONE', ( #10289, #7452, #8794, #7194, #4154 ) ) ;
#8561=CARTESIAN_POINT ( 'NONE',  ( 2.500000000000000000, 0.000000000000000000, 0.000000000000000000 ) ) ;
#8574=DIRECTION ( 'NONE',  ( 0.000000000000000000, 0.8660254037844380415, -0.5000000000000012212 ) ) ;
#8586=FACE_OUTER_BOUND ( 'NONE', #10841, .T. ) ;
#8607=CARTESIAN_POINT ( 'NONE',  ( 2.500000000000000000, -2.357898499370432610, 3.252606517456513302E-15 ) ) ;
#8609=AXIS2_PLACEMENT_3D ( 'NONE', #10278, #3449, #6771 ) ;
#8610=CARTESIAN_POINT ( 'NONE',  ( 2.500000000000000000, -2.357898499370432610, 3.252606517456513302E-15 ) ) ;
#8616=CARTESIAN_POINT ( 'NONE',  ( -31.74999999999995737, 0.000000000000000000, 0.000000000000000000 ) ) ;
#8622=EDGE_LOOP ( 'NONE', ( #1714, #5987, #5501, #383, #4559 ) ) ;
#8634=ORIENTED_EDGE ( 'NONE', *, *, #8236, .F. ) ;
#8698=CARTESIAN_POINT ( 'NONE',  ( 2.500000000000000000, -1.178949249685213863, 2.042000000000002924 ) ) ;
#8726=DIRECTION ( 'NONE',  ( -0.000000000000000000, 1.471414886128461471E-15, 1.000000000000000000 ) ) ;
#8742=DIRECTION ( 'NONE',  ( 0.000000000000000000, 0.000000000000000000, -1.000000000000000000 ) ) ;
#8743=VECTOR ( 'NONE', #8929, 1000.000000000000114 ) ;
#8762=VERTEX_POINT ( 'NONE', #8037 ) ;
#8778=EDGE_LOOP ( 'NONE', ( #5831, #9610, #9955, #6061 ) ) ;
#8794=ORIENTED_EDGE ( 'NONE', *, *, #10008, .F. ) ;
#8802=AXIS2_PLACEMENT_3D ( 'NONE', #10191, #4080, #5911 ) ;
#8808=EDGE_CURVE ( 'NONE', #2222, #1168, #2578, .T. ) ;
#8809=DIRECTION ( 'NONE',  ( 0.000000000000000000, -0.4999999999999993894, 0.8660254037844389297 ) ) ;
#8857=EDGE_CURVE ( 'NONE', #516, #7151, #7353, .T. ) ;
#8859=EDGE_CURVE ( 'NONE', #7739, #7929, #570, .T. ) ;
#8864=DIRECTION ( 'NONE',  ( -0.5000000000000051070, 0.000000000000000000, 0.8660254037844355990 ) ) ;
#8922=DIRECTION ( 'NONE',  ( -0.7071067811865306973, 0.000000000000000000, 0.7071067811865643371 ) ) ;
#8929=DIRECTION ( 'NONE',  ( 0.000000000000000000, -0.5000000000000011102, -0.8660254037844379305 ) ) ;
#8939=DIRECTION ( 'NONE',  ( 0.000000000000000000, 1.000000000000000000, -1.224646799147353207E-16 ) ) ;
#8949=EDGE_CURVE ( 'NONE', #6902, #3819, #7343, .T. ) ;
#8955=DIRECTION ( 'NONE',  ( 0.000000000000000000, 0.000000000000000000, 1.000000000000000000 ) ) ;
#9000=LINE ( 'NONE', #9940, #10388 ) ;
#9003=( LENGTH_UNIT ( ) NAMED_UNIT ( * ) SI_UNIT ( .MILLI., .METRE. ) );
#9021=FACE_OUTER_BOUND ( 'NONE', #3887, .T. ) ;
#9054=EDGE_CURVE ( 'NONE', #3173, #516, #5062, .T. ) ;
#9061=ORIENTED_EDGE ( 'NONE', *, *, #6745, .T. ) ;
#9073=EDGE_LOOP ( 'NONE', ( #1602, #2795, #2491 ) ) ;
#9086=DIRECTION ( 'NONE',  ( 0.000000000000000000, -1.287488025362403787E-15, -1.000000000000000000 ) ) ;
#9099=ORIENTED_EDGE ( 'NONE', *, *, #2772, .T. ) ;
#9113=AXIS2_PLACEMENT_3D ( 'NONE', #4720, #9086, #9141 ) ;
#9124=ORIENTED_EDGE ( 'NONE', *, *, #9972, .F. ) ;
#9138=EDGE_LOOP ( 'NONE', ( #43, #5100, #8434, #1014, #10670 ) ) ;
#9140=AXIS2_PLACEMENT_3D ( 'NONE', #10862, #637, #10982 ) ;
#9141=DIRECTION ( 'NONE',  ( 0.000000000000000000, 1.000000000000000000, -1.287488025362403787E-15 ) ) ;
#9150=ADVANCED_FACE ( 'NONE', ( #6550 ), #7183, .T. ) ;
#9151=VERTEX_POINT ( 'NONE', #5886 ) ;
#9174=LINE ( 'NONE', #1570, #5352 ) ;
#9178=FACE_OUTER_BOUND ( 'NONE', #4465, .T. ) ;
#9182=EDGE_CURVE ( 'NONE', #7578, #4891, #3279, .T. ) ;
#9253=ADVANCED_FACE ( 'NONE', ( #9330 ), #10332, .T. ) ;
#9256=ADVANCED_FACE ( 'NONE', ( #2675 ), #1953, .T. ) ;
#9266=DIRECTION ( 'NONE',  ( 0.000000000000000000, -0.5000000000000011102, -0.8660254037844379305 ) ) ;
#9278=ORIENTED_EDGE ( 'NONE', *, *, #2276, .T. ) ;
#9282=ORIENTED_EDGE ( 'NONE', *, *, #2676, .F. ) ;
#9310=ADVANCED_BREP_SHAPE_REPRESENTATION ( '', ( #1910, #308 ), #2282 ) ;
#9315=AXIS2_PLACEMENT_3D ( 'NONE', #9410, #5970, #787 ) ;
#9318=ORIENTED_EDGE ( 'NONE', *, *, #2550, .F. ) ;
#9330=FACE_OUTER_BOUND ( 'NONE', #8778, .T. ) ;
#9355=EDGE_LOOP ( 'NONE', ( #7954, #1548, #1732, #1621 ) ) ;
#9359=AXIS2_PLACEMENT_3D ( 'NONE', #8524, #8574, #2645 ) ;
#9391=CARTESIAN_POINT ( 'NONE',  ( 0.000000000000000000, 0.000000000000000000, 4.000000000000000000 ) ) ;
#9410=CARTESIAN_POINT ( 'NONE',  ( 2.500000000000000000, 2.357898499370433054, -1.951563910473907981E-15 ) ) ;
#9426=VECTOR ( 'NONE', #3481, 1000.000000000000000 ) ;
#9439=VECTOR ( 'NONE', #5376, 1000.000000000000000 ) ;
#9445=DIRECTION ( 'NONE',  ( 0.000000000000000000, 0.000000000000000000, 1.000000000000000000 ) ) ;
#9448=ORIENTED_EDGE ( 'NONE', *, *, #7918, .F. ) ;
#9459=FACE_OUTER_BOUND ( 'NONE', #7661, .T. ) ;
#9487=FACE_BOUND ( 'NONE', #10591, .T. ) ;
#9490=ORIENTED_EDGE ( 'NONE', *, *, #1940, .F. ) ;
#9514=CARTESIAN_POINT ( 'NONE',  ( 2.500000000000000000, 1.768423874527822681, -1.021000000000002794 ) ) ;
#9524=CARTESIAN_POINT ( 'NONE',  ( 2.500000000000000000, 0.000000000000000000, 2.041999999999999815 ) ) ;
#9541=CARTESIAN_POINT ( 'NONE',  ( 2.500000000000000000, 0.000000000000000000, 0.000000000000000000 ) ) ;
#9565=DIRECTION ( 'NONE',  ( 1.000000000000000000, 0.000000000000000000, 0.000000000000000000 ) ) ;
#9566=EDGE_CURVE ( 'NONE', #6542, #5182, #2664, .T. ) ;
#9592=ORIENTED_EDGE ( 'NONE', *, *, #1940, .T. ) ;
#9595=CARTESIAN_POINT ( 'NONE',  ( 0.000000000000000000, 1.178949249685213863, -2.042000000000001148 ) ) ;
#9603=DIRECTION ( 'NONE',  ( -1.000000000000000000, -0.000000000000000000, -0.000000000000000000 ) ) ;
#9607=FACE_OUTER_BOUND ( 'NONE', #8560, .T. ) ;
#9610=ORIENTED_EDGE ( 'NONE', *, *, #4038, .T. ) ;
#9617=EDGE_CURVE ( 'NONE', #9904, #6542, #7988, .T. ) ;
#9628=FACE_OUTER_BOUND ( 'NONE', #1097, .T. ) ;
#9635=LINE ( 'NONE', #2027, #668 ) ;
#9657=FACE_OUTER_BOUND ( 'NONE', #552, .T. ) ;
#9680=DIRECTION ( 'NONE',  ( 1.000000000000000000, 0.000000000000000000, 0.000000000000000000 ) ) ;
#9708=DIRECTION ( 'NONE',  ( 0.000000000000000000, -0.8660254037844390407, -0.4999999999999994449 ) ) ;
#9725=VECTOR ( 'NONE', #1282, 1000.000000000000000 ) ;
#9727=( NAMED_UNIT ( * ) SI_UNIT ( $, .STERADIAN. ) SOLID_ANGLE_UNIT ( ) );
#9742=EDGE_CURVE ( 'NONE', #4891, #4976, #5540, .T. ) ;
#9750=PRESENTATION_STYLE_ASSIGNMENT (( #3337 ) ) ;
#9771=FACE_BOUND ( 'NONE', #1774, .T. ) ;
#9775=DIRECTION ( 'NONE',  ( -1.000000000000000000, -0.000000000000000000, -0.000000000000000000 ) ) ;
#9780=PRESENTATION_STYLE_ASSIGNMENT (( #494 ) ) ;
#9781=CIRCLE ( 'NONE', #6757, 2.500000000000000888 ) ;
#9791=PRODUCT_DEFINITION_SHAPE ( 'NONE', 'NONE',  #9799 ) ;
#9798=LINE ( 'NONE', #4756, #547 ) ;
#9799=PRODUCT_DEFINITION ( 'UNKNOWN', '', #6869, #7448 ) ;
#9823=ORIENTED_EDGE ( 'NONE', *, *, #7851, .F. ) ;
#9833=LINE ( 'NONE', #9992, #600 ) ;
#9843=AXIS2_PLACEMENT_3D ( 'NONE', #1126, #397, #3743 ) ;
#9845=CARTESIAN_POINT ( 'NONE',  ( 2.500000000000000000, -1.178949249685218303, -2.041999999999998039 ) ) ;
#9859=UNCERTAINTY_MEASURE_WITH_UNIT (LENGTH_MEASURE( 1.000000000000000082E-05 ), #7500, 'distance_accuracy_value', 'NONE');
#9876=ADVANCED_FACE ( 'NONE', ( #9971 ), #614, .T. ) ;
#9891=( NAMED_UNIT ( * ) SI_UNIT ( $, .STERADIAN. ) SOLID_ANGLE_UNIT ( ) );
#9899=VECTOR ( 'NONE', #3121, 1000.000000000000000 ) ;
#9904=VERTEX_POINT ( 'NONE', #4767 ) ;
#9908=MECHANICAL_DESIGN_GEOMETRIC_PRESENTATION_REPRESENTATION('',(#5654),#7939);
#9914=DIRECTION ( 'NONE',  ( 0.000000000000000000, 0.000000000000000000, 1.000000000000000000 ) ) ;
#9920=CARTESIAN_POINT ( 'NONE',  ( 0.000000000000000000, 2.357898499370433054, -1.951563910473907981E-15 ) ) ;
#9922=CARTESIAN_POINT ( 'NONE',  ( 2.500000000000000000, 1.178949249685218525, 2.041999999999999371 ) ) ;
#9940=CARTESIAN_POINT ( 'NONE',  ( 2.500000000000000000, -2.357898499370432610, 3.252606517456513302E-15 ) ) ;
#9955=ORIENTED_EDGE ( 'NONE', *, *, #2409, .T. ) ;
#9969=CARTESIAN_POINT ( 'NONE',  ( 24.55500000000002103, 3.061616997868384620E-16, -2.500000000000001332 ) ) ;
#9971=FACE_OUTER_BOUND ( 'NONE', #5613, .T. ) ;
#9972=EDGE_CURVE ( 'NONE', #3779, #7151, #10392, .T. ) ;
#9989=ORIENTED_EDGE ( 'NONE', *, *, #7672, .F. ) ;
#9992=CARTESIAN_POINT ( 'NONE',  ( 2.500000000000000000, 1.178949249685213863, -2.042000000000001148 ) ) ;
#10008=EDGE_CURVE ( 'NONE', #2222, #2458, #10141, .T. ) ;
#10038=DIRECTION ( 'NONE',  ( 0.000000000000000000, 0.000000000000000000, -1.000000000000000000 ) ) ;
#10099=EDGE_CURVE ( 'NONE', #2929, #2222, #2083, .T. ) ;
#10106=VERTEX_POINT ( 'NONE', #1127 ) ;
#10119=ORIENTED_EDGE ( 'NONE', *, *, #1270, .T. ) ;
#10141=LINE ( 'NONE', #7085, #3292 ) ;
#10145=ADVANCED_FACE ( 'NONE', ( #7184 ), #7867, .T. ) ;
#10164=CARTESIAN_POINT ( 'NONE',  ( 0.000000000000000000, 2.357898499370433054, -1.951563910473907981E-15 ) ) ;
#10191=CARTESIAN_POINT ( 'NONE',  ( 5.000000000000004441, 0.000000000000000000, 0.000000000000000000 ) ) ;
#10233=CARTESIAN_POINT ( 'NONE',  ( 2.500000000000000000, -2.357898499370432610, 3.252606517456513302E-15 ) ) ;
#10268=ORIENTED_EDGE ( 'NONE', *, *, #9182, .T. ) ;
#10278=CARTESIAN_POINT ( 'NONE',  ( -31.74999999999995737, 0.000000000000000000, 0.000000000000000000 ) ) ;
#10288=FACE_OUTER_BOUND ( 'NONE', #1518, .T. ) ;
#10289=ORIENTED_EDGE ( 'NONE', *, *, #2550, .T. ) ;
#10303=ADVANCED_FACE ( 'NONE', ( #9021 ), #1410, .F. ) ;
#10322=VECTOR ( 'NONE', #3296, 1000.000000000000000 ) ;
#10323=DIRECTION ( 'NONE',  ( 1.000000000000000000, 0.000000000000000000, 0.000000000000000000 ) ) ;
#10332=CYLINDRICAL_SURFACE ( 'NONE', #8609, 2.500000000000000888 ) ;
#10388=VECTOR ( 'NONE', #6487, 1000.000000000000000 ) ;
#10392=CIRCLE ( 'NONE', #91, 0.2500000000000002220 ) ;
#10448=DIRECTION ( 'NONE',  ( 0.000000000000000000, -1.000000000000000000, 1.287488025362403787E-15 ) ) ;
#10477=APPLICATION_CONTEXT ( 'automotive_design' ) ;
#10582=CIRCLE ( 'NONE', #7374, 4.250000000000000000 ) ;
#10591=EDGE_LOOP ( 'NONE', ( #766, #10678 ) ) ;
#10600=CARTESIAN_POINT ( 'NONE',  ( 25.00000000000000000, 0.000000000000000000, 0.000000000000000000 ) ) ;
#10604=FACE_OUTER_BOUND ( 'NONE', #6584, .T. ) ;
#10608=VECTOR ( 'NONE', #4798, 1000.000000000000000 ) ;
#10613=CYLINDRICAL_SURFACE ( 'NONE', #4053, 4.250000000000000000 ) ;
#10619=SHAPE_REPRESENTATION_RELATIONSHIP ( 'NONE' , 'NONE' ,  #5757, #9310 ) ;
#10649=DIRECTION ( 'NONE',  ( -1.000000000000000000, -0.000000000000000000, -0.000000000000000000 ) ) ;
#10670=ORIENTED_EDGE ( 'NONE', *, *, #5380, .T. ) ;
#10678=ORIENTED_EDGE ( 'NONE', *, *, #3371, .T. ) ;
#10742=CIRCLE ( 'NONE', #5256, 2.055000000000000160 ) ;
#10747=DIRECTION ( 'NONE',  ( 0.000000000000000000, 0.000000000000000000, 1.000000000000000000 ) ) ;
#10771=EDGE_LOOP ( 'NONE', ( #9592, #2168, #4148, #353, #9278 ) ) ;
#10781=AXIS2_PLACEMENT_3D ( 'NONE', #8561, #3398, #9445 ) ;
#10785=ORIENTED_EDGE ( 'NONE', *, *, #7153, .F. ) ;
#10809=PLANE ( 'NONE',  #2592 ) ;
#10827=ORIENTED_EDGE ( 'NONE', *, *, #2276, .F. ) ;
#10841=EDGE_LOOP ( 'NONE', ( #8031, #8404, #849 ) ) ;
#10859=CARTESIAN_POINT ( 'NONE',  ( 5.200000000000002842, 0.000000000000000000, 0.000000000000000000 ) ) ;
#10862=CARTESIAN_POINT ( 'NONE',  ( -31.74999999999995737, 0.000000000000000000, 0.000000000000000000 ) ) ;
#10878=DIRECTION ( 'NONE',  ( -1.000000000000000000, -0.000000000000000000, -0.000000000000000000 ) ) ;
#10886=AXIS2_PLACEMENT_3D ( 'NONE', #3554, #4613, #2109 ) ;
#10908=ORIENTED_EDGE ( 'NONE', *, *, #5148, .T. ) ;
#10920=DIRECTION ( 'NONE',  ( 0.000000000000000000, 0.000000000000000000, -1.000000000000000000 ) ) ;
#10970=VECTOR ( 'NONE', #7748, 1000.000000000000114 ) ;
#10982=DIRECTION ( 'NONE',  ( 0.000000000000000000, 0.000000000000000000, 1.000000000000000000 ) ) ;
ENDSEC;
END-ISO-10303-21;
